ISO-10303-21;
HEADER;
/* Generated by software containing ST-Developer
 * from STEP Tools, Inc. (www.steptools.com) 
 */
/* OPTION: using custom renumber hook */

FILE_DESCRIPTION(
/* description */ ('STEP AP242 Edition 2', 'CAx-IF Rec.Pracs.---Representation and Presentation of Product Manufa
cturing Information (PMI)---4.0---2014-10-13', 'CAx-IF Rec.Pracs.---3D Tessellated Geometry---0.4---2014-09-14', '2;1', 'CAx-IF Rec.Pracs.---User Defined Attributes---1.5---2016-08-15'),
/* implementation_level */ '2;1');

FILE_NAME(
/* name */ 'angular contact ball bearing_68_bsi_BS 6267 ABB - 4815 - 18,SI,NC,18__68__ DE    23193__PD18845.step',
/* time_stamp */ '2026-10-09T00:23:50Z',
/* author */ (''),
/* organization */ (''),
/* preprocessor_version */ 'ST-DEVELOPER v20',
/* originating_system */ 'ONSHAPE BY PTC INC, 1.221',
/* authorisation */ '  ');

FILE_SCHEMA (('AP242_MANAGED_MODEL_BASED_3D_ENGINEERING_MIM_LF { 1 0 10303 442 3 1 4 }'));
ENDSEC;

DATA;
#64=TOROIDAL_SURFACE('',#8653,0.0117000000001705,0.000300000000224998);
#65=TOROIDAL_SURFACE('',#8662,0.0117000000001705,0.000300000000224998);
#66=TOROIDAL_SURFACE('',#8664,0.00974999999980933,0.00134999999974855);
#67=TOROIDAL_SURFACE('',#8665,0.00974999999980933,0.00134999999974855);
#68=TOROIDAL_SURFACE('',#8676,0.00975000000019067,0.00134999999974855);
#69=TOROIDAL_SURFACE('',#8677,0.00975000000019067,0.00134999999974855);
#70=TOROIDAL_SURFACE('',#8679,0.00779999999982954,0.000300000000224997);
#71=TOROIDAL_SURFACE('',#8680,0.00779999999982954,0.000300000000224997);
#72=TOROIDAL_SURFACE('',#8689,0.00779999999982955,0.000300000000225003);
#73=TOROIDAL_SURFACE('',#8690,0.00779999999982955,0.000300000000225003);
#147=SHAPE_REPRESENTATION_RELATIONSHIP('','',#8237,#153);
#153=ADVANCED_BREP_SHAPE_REPRESENTATION('',(#8223),#18815);
#523=B_SPLINE_CURVE_WITH_KNOTS('',3,(#13521,#13522,#13523,#13524,#13525,
#13526,#13527,#13528,#13529,#13530,#13531),.UNSPECIFIED.,.F.,.F.,(4,1,1,
1,1,1,1,1,4),(6.5285800070357E-11,0.125000000047178,0.25000000002907,0.375000000010962,
0.499999999992854,0.624999999974746,0.749999999956638,0.87499999993853,
0.999999999920422),.UNSPECIFIED.);
#524=B_SPLINE_CURVE_WITH_KNOTS('',3,(#13541,#13542,#13543,#13544,#13545,
#13546,#13547,#13548,#13549,#13550,#13551),.UNSPECIFIED.,.F.,.F.,(4,1,1,
1,1,1,1,1,4),(0.,0.125,0.25,0.375,0.5,0.625,0.75,0.875,1.),
 .UNSPECIFIED.);
#525=B_SPLINE_CURVE_WITH_KNOTS('',3,(#13556,#13557,#13558,#13559,#13560,
#13561,#13562,#13563,#13564,#13565,#13566),.UNSPECIFIED.,.F.,.F.,(4,1,1,
1,1,1,1,1,4),(0.,0.125,0.25,0.375,0.5,0.625,0.75,0.875,1.),
 .UNSPECIFIED.);
#526=B_SPLINE_CURVE_WITH_KNOTS('',3,(#13574,#13575,#13576,#13577,#13578),
 .UNSPECIFIED.,.F.,.F.,(4,1,4),(0.,0.499999978485393,0.999999956970785),
 .UNSPECIFIED.);
#527=B_SPLINE_CURVE_WITH_KNOTS('',3,(#13580,#13581,#13582,#13583,#13584,
#13585,#13586,#13587,#13588,#13589,#13590),.UNSPECIFIED.,.F.,.F.,(4,1,1,
1,1,1,1,1,4),(1.08159811971616E-10,0.125000000086479,0.250000000064798,
0.375000000043118,0.500000000021437,0.624999999999756,0.749999999978076,
0.874999999956395,0.999999999934714),.UNSPECIFIED.);
#528=B_SPLINE_CURVE_WITH_KNOTS('',3,(#13592,#13593,#13594,#13595,#13596),
 .UNSPECIFIED.,.F.,.F.,(4,1,4),(4.3029215375297E-8,0.49999997764101,0.999999912252804),
 .UNSPECIFIED.);
#529=B_SPLINE_CURVE_WITH_KNOTS('',3,(#13606,#13607,#13608,#13609,#13610,
#13611,#13612,#13613,#13614,#13615,#13616),.UNSPECIFIED.,.F.,.F.,(4,1,1,
1,1,1,1,1,4),(0.,0.125,0.25,0.375,0.5,0.625,0.75,0.875,1.),
 .UNSPECIFIED.);
#530=B_SPLINE_CURVE_WITH_KNOTS('',3,(#13626,#13627,#13628,#13629,#13630),
 .UNSPECIFIED.,.F.,.F.,(4,1,4),(2.91751359515211E-8,0.499999949957411,0.999999870739685),
 .UNSPECIFIED.);
#531=B_SPLINE_CURVE_WITH_KNOTS('',3,(#13632,#13633,#13634,#13635,#13636),
 .UNSPECIFIED.,.F.,.F.,(4,1,4),(0.,0.499999985412432,0.999999970824864),
 .UNSPECIFIED.);
#532=B_SPLINE_CURVE_WITH_KNOTS('',3,(#13638,#13639,#13640,#13641,#13642,
#13643,#13644,#13645,#13646,#13647,#13648),.UNSPECIFIED.,.F.,.F.,(4,1,1,
1,1,1,1,1,4),(2.37190894409548E-10,0.125000000203969,0.250000000170748,
0.375000000137526,0.500000000104304,0.625000000071083,0.750000000037861,
0.875000000004639,0.999999999971418),.UNSPECIFIED.);
#533=B_SPLINE_CURVE_WITH_KNOTS('',3,(#13652,#13653,#13654,#13655),
 .UNSPECIFIED.,.F.,.F.,(4,4),(0.,1.),.UNSPECIFIED.);
#534=B_SPLINE_CURVE_WITH_KNOTS('',3,(#13657,#13658,#13659,#13660),
 .UNSPECIFIED.,.F.,.F.,(4,4),(0.,1.),.UNSPECIFIED.);
#535=B_SPLINE_CURVE_WITH_KNOTS('',3,(#13662,#13663,#13664,#13665,#13666,
#13667,#13668),.UNSPECIFIED.,.F.,.F.,(4,1,1,1,4),(1.82135136395292E-10,
0.25000000012028,0.500000000058424,0.749999999996569,0.999999999934713),
 .UNSPECIFIED.);
#536=B_SPLINE_CURVE_WITH_KNOTS('',3,(#13675,#13676,#13677,#13678,#13679,
#13680,#13681),.UNSPECIFIED.,.F.,.F.,(4,1,1,1,4),(0.,0.25,0.5,0.75,1.),
 .UNSPECIFIED.);
#537=B_SPLINE_CURVE_WITH_KNOTS('',3,(#13691,#13692,#13693,#13694),
 .UNSPECIFIED.,.F.,.F.,(4,4),(0.,1.),.UNSPECIFIED.);
#538=B_SPLINE_CURVE_WITH_KNOTS('',3,(#13695,#13696,#13697,#13698),
 .UNSPECIFIED.,.F.,.F.,(4,4),(0.,1.),.UNSPECIFIED.);
#1043=PLANE('',#8656);
#1044=PLANE('',#8667);
#1045=PLANE('',#8673);
#1046=PLANE('',#8686);
#2190=ORIENTED_EDGE('',*,*,#4016,.T.);
#2191=ORIENTED_EDGE('',*,*,#4017,.T.);
#2192=ORIENTED_EDGE('',*,*,#4018,.T.);
#2193=ORIENTED_EDGE('',*,*,#4018,.F.);
#2194=ORIENTED_EDGE('',*,*,#4019,.T.);
#2195=ORIENTED_EDGE('',*,*,#4020,.T.);
#2196=ORIENTED_EDGE('',*,*,#4021,.T.);
#2197=ORIENTED_EDGE('',*,*,#4017,.F.);
#2198=ORIENTED_EDGE('',*,*,#4016,.F.);
#2199=ORIENTED_EDGE('',*,*,#4019,.F.);
#2200=ORIENTED_EDGE('',*,*,#4022,.F.);
#2201=ORIENTED_EDGE('',*,*,#4023,.F.);
#2202=ORIENTED_EDGE('',*,*,#4024,.T.);
#2203=ORIENTED_EDGE('',*,*,#4021,.F.);
#2204=ORIENTED_EDGE('',*,*,#4020,.F.);
#2205=ORIENTED_EDGE('',*,*,#4025,.T.);
#2206=ORIENTED_EDGE('',*,*,#4026,.T.);
#2207=ORIENTED_EDGE('',*,*,#4027,.T.);
#2208=ORIENTED_EDGE('',*,*,#4022,.T.);
#2209=ORIENTED_EDGE('',*,*,#4028,.T.);
#2210=ORIENTED_EDGE('',*,*,#4025,.F.);
#2211=ORIENTED_EDGE('',*,*,#4023,.T.);
#2212=ORIENTED_EDGE('',*,*,#4027,.F.);
#2213=ORIENTED_EDGE('',*,*,#4024,.F.);
#2214=ORIENTED_EDGE('',*,*,#4029,.T.);
#2215=ORIENTED_EDGE('',*,*,#4028,.F.);
#2216=ORIENTED_EDGE('',*,*,#4026,.F.);
#2217=ORIENTED_EDGE('',*,*,#4030,.T.);
#2218=ORIENTED_EDGE('',*,*,#4031,.F.);
#2219=ORIENTED_EDGE('',*,*,#4032,.F.);
#2220=ORIENTED_EDGE('',*,*,#4029,.F.);
#2221=ORIENTED_EDGE('',*,*,#4030,.F.);
#2222=ORIENTED_EDGE('',*,*,#4033,.T.);
#2223=ORIENTED_EDGE('',*,*,#4034,.T.);
#2224=ORIENTED_EDGE('',*,*,#4035,.T.);
#2225=ORIENTED_EDGE('',*,*,#4031,.T.);
#2226=ORIENTED_EDGE('',*,*,#4036,.T.);
#2227=ORIENTED_EDGE('',*,*,#4037,.T.);
#2228=ORIENTED_EDGE('',*,*,#4032,.T.);
#2229=ORIENTED_EDGE('',*,*,#4035,.F.);
#2230=ORIENTED_EDGE('',*,*,#4038,.T.);
#2231=ORIENTED_EDGE('',*,*,#4036,.F.);
#2232=ORIENTED_EDGE('',*,*,#4039,.T.);
#2233=ORIENTED_EDGE('',*,*,#4034,.F.);
#2234=ORIENTED_EDGE('',*,*,#4040,.T.);
#2235=ORIENTED_EDGE('',*,*,#4041,.T.);
#2236=ORIENTED_EDGE('',*,*,#4033,.F.);
#2237=ORIENTED_EDGE('',*,*,#4039,.F.);
#2238=ORIENTED_EDGE('',*,*,#4042,.T.);
#2239=ORIENTED_EDGE('',*,*,#4040,.F.);
#2240=ORIENTED_EDGE('',*,*,#4043,.T.);
#2241=ORIENTED_EDGE('',*,*,#4037,.F.);
#2242=ORIENTED_EDGE('',*,*,#4038,.F.);
#2243=ORIENTED_EDGE('',*,*,#4041,.F.);
#2244=ORIENTED_EDGE('',*,*,#4042,.F.);
#2245=ORIENTED_EDGE('',*,*,#4044,.F.);
#2246=ORIENTED_EDGE('',*,*,#4045,.F.);
#2247=ORIENTED_EDGE('',*,*,#4043,.F.);
#2248=ORIENTED_EDGE('',*,*,#4046,.T.);
#2249=ORIENTED_EDGE('',*,*,#4047,.T.);
#2250=ORIENTED_EDGE('',*,*,#4048,.T.);
#2251=ORIENTED_EDGE('',*,*,#4044,.T.);
#2252=ORIENTED_EDGE('',*,*,#4049,.T.);
#2253=ORIENTED_EDGE('',*,*,#4047,.F.);
#2254=ORIENTED_EDGE('',*,*,#4045,.T.);
#2255=ORIENTED_EDGE('',*,*,#4048,.F.);
#2256=ORIENTED_EDGE('',*,*,#4046,.F.);
#2257=ORIENTED_EDGE('',*,*,#4049,.F.);
#4016=EDGE_CURVE('',#5023,#5024,#523,.T.);
#4017=EDGE_CURVE('',#5024,#5023,#5679,.T.);
#4018=EDGE_CURVE('',#5025,#5025,#5680,.F.);
#4019=EDGE_CURVE('',#5026,#5026,#5681,.F.);
#4020=EDGE_CURVE('',#5027,#5028,#524,.F.);
#4021=EDGE_CURVE('',#5028,#5027,#5682,.T.);
#4022=EDGE_CURVE('',#5029,#5030,#525,.F.);
#4023=EDGE_CURVE('',#5030,#5029,#5683,.T.);
#4024=EDGE_CURVE('',#5031,#5031,#5684,.T.);
#4025=EDGE_CURVE('',#5030,#5032,#526,.T.);
#4026=EDGE_CURVE('',#5032,#5033,#527,.T.);
#4027=EDGE_CURVE('',#5033,#5029,#528,.T.);
#4028=EDGE_CURVE('',#5033,#5032,#5685,.F.);
#4029=EDGE_CURVE('',#5034,#5034,#5686,.T.);
#4030=EDGE_CURVE('',#5035,#5035,#5687,.F.);
#4031=EDGE_CURVE('',#5036,#5037,#529,.F.);
#4032=EDGE_CURVE('',#5037,#5036,#5688,.F.);
#4033=EDGE_CURVE('',#5038,#5039,#5689,.F.);
#4034=EDGE_CURVE('',#5039,#5038,#5690,.F.);
#4035=EDGE_CURVE('',#5040,#5036,#530,.T.);
#4036=EDGE_CURVE('',#5037,#5041,#531,.T.);
#4037=EDGE_CURVE('',#5041,#5040,#532,.T.);
#4038=EDGE_CURVE('',#5040,#5041,#5691,.T.);
#4039=EDGE_CURVE('',#5042,#5038,#533,.T.);
#4040=EDGE_CURVE('',#5039,#5043,#534,.T.);
#4041=EDGE_CURVE('',#5043,#5042,#535,.T.);
#4042=EDGE_CURVE('',#5042,#5043,#5692,.F.);
#4043=EDGE_CURVE('',#5044,#5044,#5693,.T.);
#4044=EDGE_CURVE('',#5045,#5046,#536,.F.);
#4045=EDGE_CURVE('',#5046,#5045,#5694,.T.);
#4046=EDGE_CURVE('',#5047,#5048,#5695,.T.);
#4047=EDGE_CURVE('',#5048,#5047,#5696,.T.);
#4048=EDGE_CURVE('',#5048,#5045,#537,.T.);
#4049=EDGE_CURVE('',#5046,#5047,#538,.T.);
#5023=VERTEX_POINT('',#13532);
#5024=VERTEX_POINT('',#13533);
#5025=VERTEX_POINT('',#13536);
#5026=VERTEX_POINT('',#13539);
#5027=VERTEX_POINT('',#13552);
#5028=VERTEX_POINT('',#13553);
#5029=VERTEX_POINT('',#13567);
#5030=VERTEX_POINT('',#13568);
#5031=VERTEX_POINT('',#13572);
#5032=VERTEX_POINT('',#13579);
#5033=VERTEX_POINT('',#13591);
#5034=VERTEX_POINT('',#13601);
#5035=VERTEX_POINT('',#13604);
#5036=VERTEX_POINT('',#13617);
#5037=VERTEX_POINT('',#13618);
#5038=VERTEX_POINT('',#13622);
#5039=VERTEX_POINT('',#13623);
#5040=VERTEX_POINT('',#13631);
#5041=VERTEX_POINT('',#13637);
#5042=VERTEX_POINT('',#13656);
#5043=VERTEX_POINT('',#13661);
#5044=VERTEX_POINT('',#13673);
#5045=VERTEX_POINT('',#13682);
#5046=VERTEX_POINT('',#13683);
#5047=VERTEX_POINT('',#13687);
#5048=VERTEX_POINT('',#13688);
#5679=CIRCLE('',#8654,0.0120000000003955);
#5680=CIRCLE('',#8655,0.0117000000001921);
#5681=CIRCLE('',#8657,0.01065);
#5682=CIRCLE('',#8659,0.012);
#5683=CIRCLE('',#8661,0.0106499999992724);
#5684=CIRCLE('',#8663,0.0117000000001921);
#5685=CIRCLE('',#8666,0.00842500000016944);
#5686=CIRCLE('',#8668,0.011075);
#5687=CIRCLE('',#8670,0.008425);
#5688=CIRCLE('',#8672,0.0110749999998306);
#5689=CIRCLE('',#8674,0.00779999999980785);
#5690=CIRCLE('',#8675,0.00779999999980785);
#5691=CIRCLE('',#8678,0.00885000000072759);
#5692=CIRCLE('',#8681,0.00749999999960454);
#5693=CIRCLE('',#8683,0.00885);
#5694=CIRCLE('',#8685,0.00749999999960454);
#5695=CIRCLE('',#8687,0.00779999999980785);
#5696=CIRCLE('',#8688,0.00779999999980785);
#6231=EDGE_LOOP('',(#2190,#2191));
#6232=EDGE_LOOP('',(#2192));
#6233=EDGE_LOOP('',(#2193));
#6234=EDGE_LOOP('',(#2194));
#6235=EDGE_LOOP('',(#2195,#2196));
#6236=EDGE_LOOP('',(#2197,#2198));
#6237=EDGE_LOOP('',(#2199));
#6238=EDGE_LOOP('',(#2200,#2201));
#6239=EDGE_LOOP('',(#2202));
#6240=EDGE_LOOP('',(#2203,#2204));
#6241=EDGE_LOOP('',(#2205,#2206,#2207,#2208));
#6242=EDGE_LOOP('',(#2209,#2210,#2211,#2212));
#6243=EDGE_LOOP('',(#2213));
#6244=EDGE_LOOP('',(#2214));
#6245=EDGE_LOOP('',(#2215,#2216));
#6246=EDGE_LOOP('',(#2217));
#6247=EDGE_LOOP('',(#2218,#2219));
#6248=EDGE_LOOP('',(#2220));
#6249=EDGE_LOOP('',(#2221));
#6250=EDGE_LOOP('',(#2222,#2223));
#6251=EDGE_LOOP('',(#2224,#2225,#2226,#2227));
#6252=EDGE_LOOP('',(#2228,#2229,#2230,#2231));
#6253=EDGE_LOOP('',(#2232,#2233,#2234,#2235));
#6254=EDGE_LOOP('',(#2236,#2237,#2238,#2239));
#6255=EDGE_LOOP('',(#2240));
#6256=EDGE_LOOP('',(#2241,#2242));
#6257=EDGE_LOOP('',(#2243,#2244));
#6258=EDGE_LOOP('',(#2245,#2246));
#6259=EDGE_LOOP('',(#2247));
#6260=EDGE_LOOP('',(#2248,#2249));
#6261=EDGE_LOOP('',(#2250,#2251,#2252,#2253));
#6262=EDGE_LOOP('',(#2254,#2255,#2256,#2257));
#6992=FACE_BOUND('',#6231,.T.);
#6993=FACE_BOUND('',#6232,.T.);
#6994=FACE_BOUND('',#6233,.T.);
#6995=FACE_BOUND('',#6234,.T.);
#6996=FACE_BOUND('',#6235,.T.);
#6997=FACE_BOUND('',#6236,.T.);
#6998=FACE_BOUND('',#6237,.T.);
#6999=FACE_BOUND('',#6238,.T.);
#7000=FACE_BOUND('',#6239,.T.);
#7001=FACE_BOUND('',#6240,.T.);
#7002=FACE_BOUND('',#6241,.T.);
#7003=FACE_BOUND('',#6242,.T.);
#7004=FACE_BOUND('',#6243,.T.);
#7005=FACE_BOUND('',#6244,.T.);
#7006=FACE_BOUND('',#6245,.T.);
#7007=FACE_BOUND('',#6246,.T.);
#7008=FACE_BOUND('',#6247,.T.);
#7009=FACE_BOUND('',#6248,.T.);
#7010=FACE_BOUND('',#6249,.T.);
#7011=FACE_BOUND('',#6250,.T.);
#7012=FACE_BOUND('',#6251,.T.);
#7013=FACE_BOUND('',#6252,.T.);
#7014=FACE_BOUND('',#6253,.T.);
#7015=FACE_BOUND('',#6254,.T.);
#7016=FACE_BOUND('',#6255,.T.);
#7017=FACE_BOUND('',#6256,.T.);
#7018=FACE_BOUND('',#6257,.T.);
#7019=FACE_BOUND('',#6258,.T.);
#7020=FACE_BOUND('',#6259,.T.);
#7021=FACE_BOUND('',#6260,.T.);
#7022=FACE_BOUND('',#6261,.T.);
#7023=FACE_BOUND('',#6262,.T.);
#7517=CYLINDRICAL_SURFACE('',#8658,0.012);
#7518=CYLINDRICAL_SURFACE('',#8660,0.01065);
#7519=CYLINDRICAL_SURFACE('',#8669,0.008425);
#7520=CYLINDRICAL_SURFACE('',#8671,0.011075);
#7521=CYLINDRICAL_SURFACE('',#8682,0.00885);
#7522=CYLINDRICAL_SURFACE('',#8684,0.0075);
#7893=ADVANCED_FACE('',(#6992,#6993),#64,.T.);
#7894=ADVANCED_FACE('',(#6994,#6995),#1043,.T.);
#7895=ADVANCED_FACE('',(#6996,#6997),#7517,.T.);
#7896=ADVANCED_FACE('',(#6998,#6999),#7518,.F.);
#7897=ADVANCED_FACE('',(#7000,#7001),#65,.T.);
#7898=ADVANCED_FACE('',(#7002),#66,.T.);
#7899=ADVANCED_FACE('',(#7003),#67,.T.);
#7900=ADVANCED_FACE('',(#7004,#7005),#1044,.T.);
#7901=ADVANCED_FACE('',(#7006,#7007),#7519,.T.);
#7902=ADVANCED_FACE('',(#7008,#7009),#7520,.F.);
#7903=ADVANCED_FACE('',(#7010,#7011),#1045,.T.);
#7904=ADVANCED_FACE('',(#7012),#68,.T.);
#7905=ADVANCED_FACE('',(#7013),#69,.T.);
#7906=ADVANCED_FACE('',(#7014),#70,.T.);
#7907=ADVANCED_FACE('',(#7015),#71,.T.);
#7908=ADVANCED_FACE('',(#7016,#7017),#7521,.T.);
#7909=ADVANCED_FACE('',(#7018,#7019),#7522,.F.);
#7910=ADVANCED_FACE('',(#7020,#7021),#1046,.T.);
#7911=ADVANCED_FACE('',(#7022),#72,.T.);
#7912=ADVANCED_FACE('',(#7023),#73,.T.);
#8172=CLOSED_SHELL('',(#7893,#7894,#7895,#7896,#7897,#7898,#7899,#7900,
#7901,#7902,#7903,#7904,#7905,#7906,#7907,#7908,#7909,#7910,#7911,#7912));
#8178=STYLED_ITEM('',(#8184),#8223);
#8184=PRESENTATION_STYLE_ASSIGNMENT((#8190));
#8190=SURFACE_STYLE_USAGE(.BOTH.,#8196);
#8196=SURFACE_SIDE_STYLE('',(#8202));
#8202=SURFACE_STYLE_FILL_AREA(#8208);
#8208=FILL_AREA_STYLE('',(#8214));
#8214=FILL_AREA_STYLE_COLOUR('',#8217);
#8217=COLOUR_RGB('', 0.72549020, 0.75294118, 0.79215686);
#8223=MANIFOLD_SOLID_BREP(
'angular contact ball bearing_68_bsi_BS 6267 ABB - 4815 - 18,SI,NC,18_
68__ DE    23193',#8172);
#8230=SHAPE_DEFINITION_REPRESENTATION(#18836,#8237);
#8237=SHAPE_REPRESENTATION(
'angular contact ball bearing_68_bsi_BS 6267 ABB - 4815 - 18,SI,NC,18_
68__ DE    23193',(#8239),#18815);
#8239=AXIS2_PLACEMENT_3D('',#11098,#9192,#9193);
#8653=AXIS2_PLACEMENT_3D('',#13520,#10020,#10021);
#8654=AXIS2_PLACEMENT_3D('',#13534,#10022,#10023);
#8655=AXIS2_PLACEMENT_3D('',#13535,#10024,#10025);
#8656=AXIS2_PLACEMENT_3D('',#13537,#10026,#10027);
#8657=AXIS2_PLACEMENT_3D('',#13538,#10028,#10029);
#8658=AXIS2_PLACEMENT_3D('',#13540,#10030,#10031);
#8659=AXIS2_PLACEMENT_3D('',#13554,#10032,#10033);
#8660=AXIS2_PLACEMENT_3D('',#13555,#10034,#10035);
#8661=AXIS2_PLACEMENT_3D('',#13569,#10036,#10037);
#8662=AXIS2_PLACEMENT_3D('',#13570,#10038,#10039);
#8663=AXIS2_PLACEMENT_3D('',#13571,#10040,#10041);
#8664=AXIS2_PLACEMENT_3D('',#13573,#10042,#10043);
#8665=AXIS2_PLACEMENT_3D('',#13597,#10044,#10045);
#8666=AXIS2_PLACEMENT_3D('',#13598,#10046,#10047);
#8667=AXIS2_PLACEMENT_3D('',#13599,#10048,#10049);
#8668=AXIS2_PLACEMENT_3D('',#13600,#10050,#10051);
#8669=AXIS2_PLACEMENT_3D('',#13602,#10052,#10053);
#8670=AXIS2_PLACEMENT_3D('',#13603,#10054,#10055);
#8671=AXIS2_PLACEMENT_3D('',#13605,#10056,#10057);
#8672=AXIS2_PLACEMENT_3D('',#13619,#10058,#10059);
#8673=AXIS2_PLACEMENT_3D('',#13620,#10060,#10061);
#8674=AXIS2_PLACEMENT_3D('',#13621,#10062,#10063);
#8675=AXIS2_PLACEMENT_3D('',#13624,#10064,#10065);
#8676=AXIS2_PLACEMENT_3D('',#13625,#10066,#10067);
#8677=AXIS2_PLACEMENT_3D('',#13649,#10068,#10069);
#8678=AXIS2_PLACEMENT_3D('',#13650,#10070,#10071);
#8679=AXIS2_PLACEMENT_3D('',#13651,#10072,#10073);
#8680=AXIS2_PLACEMENT_3D('',#13669,#10074,#10075);
#8681=AXIS2_PLACEMENT_3D('',#13670,#10076,#10077);
#8682=AXIS2_PLACEMENT_3D('',#13671,#10078,#10079);
#8683=AXIS2_PLACEMENT_3D('',#13672,#10080,#10081);
#8684=AXIS2_PLACEMENT_3D('',#13674,#10082,#10083);
#8685=AXIS2_PLACEMENT_3D('',#13684,#10084,#10085);
#8686=AXIS2_PLACEMENT_3D('',#13685,#10086,#10087);
#8687=AXIS2_PLACEMENT_3D('',#13686,#10088,#10089);
#8688=AXIS2_PLACEMENT_3D('',#13689,#10090,#10091);
#8689=AXIS2_PLACEMENT_3D('',#13690,#10092,#10093);
#8690=AXIS2_PLACEMENT_3D('',#13699,#10094,#10095);
#9192=DIRECTION('',(0.,0.,1.));
#9193=DIRECTION('',(1.,0.,0.));
#10020=DIRECTION('',(1.,-4.75612924231451E-12,-4.0043073372981E-18));
#10021=DIRECTION('',(4.75612924231451E-12,1.,0.));
#10022=DIRECTION('',(1.,-4.75612924231451E-12,-4.0043073372981E-18));
#10023=DIRECTION('',(4.75612924231451E-12,1.,0.));
#10024=DIRECTION('',(1.,-4.75612924231451E-12,-4.0043073372981E-18));
#10025=DIRECTION('',(4.75612924231451E-12,1.,0.));
#10026=DIRECTION('',(1.,4.22825609356439E-17,-4.00585564781671E-17));
#10027=DIRECTION('',(-4.22825609356439E-17,1.,0.));
#10028=DIRECTION('',(1.,0.,-1.2509555207044E-16));
#10029=DIRECTION('',(-1.2509555207044E-16,0.,-1.));
#10030=DIRECTION('',(1.,0.,-7.40148683083438E-17));
#10031=DIRECTION('',(-7.40148683083438E-17,0.,-1.));
#10032=DIRECTION('',(1.,0.,-7.40148683083438E-17));
#10033=DIRECTION('',(-7.40148683083438E-17,0.,-1.));
#10034=DIRECTION('',(1.,0.,-1.2509555207044E-16));
#10035=DIRECTION('',(-1.2509555207044E-16,0.,-1.));
#10036=DIRECTION('',(1.,-8.51933299579803E-12,-1.51031137741696E-17));
#10037=DIRECTION('',(8.51933299579803E-12,1.,0.));
#10038=DIRECTION('',(1.,4.75611052379189E-12,2.67348976061206E-17));
#10039=DIRECTION('',(-4.75611052379189E-12,1.,0.));
#10040=DIRECTION('',(1.,4.75611052379189E-12,2.67348976061206E-17));
#10041=DIRECTION('',(-4.75611052379189E-12,1.,0.));
#10042=DIRECTION('',(1.,8.51931011104313E-12,9.10429714682885E-18));
#10043=DIRECTION('',(-8.51931011104313E-12,1.,0.));
#10044=DIRECTION('',(1.,-8.51933299579803E-12,-1.51031137741696E-17));
#10045=DIRECTION('',(8.51933299579803E-12,1.,0.));
#10046=DIRECTION('',(1.,-8.51933299579803E-12,-1.51031137741696E-17));
#10047=DIRECTION('',(8.51933299579803E-12,1.,0.));
#10048=DIRECTION('',(-1.,4.22825609356439E-17,4.00585564781671E-17));
#10049=DIRECTION('',(-4.22825609356439E-17,-1.,0.));
#10050=DIRECTION('',(1.,0.,0.));
#10051=DIRECTION('',(0.,0.,-1.));
#10052=DIRECTION('',(1.,0.,-7.90663281632159E-17));
#10053=DIRECTION('',(-7.90663281632159E-17,0.,-1.));
#10054=DIRECTION('',(1.,0.,-7.90663281632159E-17));
#10055=DIRECTION('',(-7.90663281632159E-17,0.,-1.));
#10056=DIRECTION('',(1.,0.,0.));
#10057=DIRECTION('',(0.,0.,-1.));
#10058=DIRECTION('',(1.,8.51953932343756E-12,7.17449131436051E-18));
#10059=DIRECTION('',(-8.51953932343756E-12,1.,0.));
#10060=DIRECTION('',(1.,5.87188086584048E-17,-5.56302802130048E-17));
#10061=DIRECTION('',(-5.87188086584048E-17,1.,0.));
#10062=DIRECTION('',(1.,-7.13444545520919E-12,-2.65134118218329E-17));
#10063=DIRECTION('',(7.13444545520919E-12,1.,0.));
#10064=DIRECTION('',(1.,7.13442257045429E-12,2.86761022065096E-17));
#10065=DIRECTION('',(-7.13442257045429E-12,1.,0.));
#10066=DIRECTION('',(1.,-8.51956220819246E-12,-1.01389396052301E-18));
#10067=DIRECTION('',(8.51956220819246E-12,1.,0.));
#10068=DIRECTION('',(1.,8.51953932343756E-12,7.17449131436051E-18));
#10069=DIRECTION('',(-8.51953932343756E-12,1.,0.));
#10070=DIRECTION('',(1.,8.51953932343756E-12,7.17449131436051E-18));
#10071=DIRECTION('',(-8.51953932343756E-12,1.,0.));
#10072=DIRECTION('',(1.,7.13442257045429E-12,2.86761022065096E-17));
#10073=DIRECTION('',(-7.13442257045429E-12,1.,0.));
#10074=DIRECTION('',(1.,-7.13444545520919E-12,-2.65134118218329E-17));
#10075=DIRECTION('',(7.13444545520919E-12,1.,0.));
#10076=DIRECTION('',(1.,-7.13444545520919E-12,-2.65134118218329E-17));
#10077=DIRECTION('',(7.13444545520919E-12,1.,0.));
#10078=DIRECTION('',(1.,0.,0.));
#10079=DIRECTION('',(0.,0.,-1.));
#10080=DIRECTION('',(1.,0.,0.));
#10081=DIRECTION('',(0.,0.,-1.));
#10082=DIRECTION('',(1.,0.,-1.1842378929335E-16));
#10083=DIRECTION('',(-1.1842378929335E-16,0.,-1.));
#10084=DIRECTION('',(1.,7.13444719404544E-12,-2.88724849698279E-17));
#10085=DIRECTION('',(-7.13444719404544E-12,1.,0.));
#10086=DIRECTION('',(-1.,5.58989788640793E-17,5.29587695813052E-17));
#10087=DIRECTION('',(-5.58989788640793E-17,-1.,0.));
#10088=DIRECTION('',(1.,7.13444719404544E-12,-2.88724849698279E-17));
#10089=DIRECTION('',(-7.13444719404544E-12,1.,0.));
#10090=DIRECTION('',(1.,-7.13447007880035E-12,4.01455929805839E-17));
#10091=DIRECTION('',(7.13447007880035E-12,1.,0.));
#10092=DIRECTION('',(1.,-7.13447007880035E-12,4.01455929805839E-17));
#10093=DIRECTION('',(7.13447007880035E-12,1.,0.));
#10094=DIRECTION('',(1.,7.13444719404544E-12,-2.88724849698279E-17));
#10095=DIRECTION('',(-7.13444719404544E-12,1.,0.));
#11098=CARTESIAN_POINT('',(0.,0.,0.));
#13520=CARTESIAN_POINT('',(0.00420000000011192,-3.50899506067413E-13,5.47386837469071E-19));
#13521=CARTESIAN_POINT('',(0.00420000000019215,-2.46124009164679E-12,0.0120000000003955));
#13522=CARTESIAN_POINT('',(0.00420000000019962,-0.00157079632905111,0.0120000000000274));
#13523=CARTESIAN_POINT('',(0.00420000000021455,-0.00471165671129617,0.0113751824584622));
#13524=CARTESIAN_POINT('',(0.00420000000023355,-0.00870621415729384,0.00870618773365808));
#13525=CARTESIAN_POINT('',(0.00420000000024625,-0.0113751749099263,0.00471175484862072));
#13526=CARTESIAN_POINT('',(0.00420000000025071,-0.0123124125450508,2.76378563580788E-13));
#13527=CARTESIAN_POINT('',(0.00420000000024625,-0.0113751749101378,-0.00471175484810999));
#13528=CARTESIAN_POINT('',(0.00420000000023355,-0.00870621415768473,-0.00870618773326719));
#13529=CARTESIAN_POINT('',(0.00420000000021456,-0.0047116567118069,-0.0113751824582506));
#13530=CARTESIAN_POINT('',(0.00420000000019962,-0.00157079632958987,-0.0119999999999568));
#13531=CARTESIAN_POINT('',(0.00420000000019215,-3.00000140206592E-12,-0.0120000000003955));
#13532=CARTESIAN_POINT('',(0.00419999987509607,-2.46123887461207E-12,0.0120000000001977));
#13533=CARTESIAN_POINT('',(0.00419999987509607,-3.00000082519295E-12,-0.0120000000001977));
#13534=CARTESIAN_POINT('',(0.00420000000019215,-3.50899506067795E-13,5.47386837468749E-19));
#13535=CARTESIAN_POINT('',(0.00450000000033692,-3.52326344841177E-13,5.4618554526698E-19));
#13536=CARTESIAN_POINT('',(0.00450000000039257,0.0116999999998398,5.4618554526698E-19));
#13537=CARTESIAN_POINT('',(0.0045,-5.3776427755281E-19,-1.47451495458029E-19));
#13538=CARTESIAN_POINT('',(0.0045,0.,-3.14458944017069E-18));
#13539=CARTESIAN_POINT('',(0.0045,0.,-0.01065));
#13540=CARTESIAN_POINT('',(-0.0206375,0.,-4.67643299434448E-52));
#13541=CARTESIAN_POINT('',(-0.0042,-5.15503667236967E-12,-0.012));
#13542=CARTESIAN_POINT('',(-0.0042,-0.00157079633140504,-0.0119999999993252));
#13543=CARTESIAN_POINT('',(-0.0042,-0.00471165671284908,-0.0113751824573995));
#13544=CARTESIAN_POINT('',(-0.0042,-0.0087062141577214,-0.00870618773284344));
#13545=CARTESIAN_POINT('',(-0.0042,-0.0113751749096969,-0.00471175484865801));
#13546=CARTESIAN_POINT('',(-0.0042,-0.0123124125448799,-1.41974949723703E-12));
#13547=CARTESIAN_POINT('',(-0.0042,-0.0113751749107835,0.00471175484603467));
#13548=CARTESIAN_POINT('',(-0.0042,-0.00870621415972922,0.0087061877308356));
#13549=CARTESIAN_POINT('',(-0.0042,-0.00471165671547242,0.0113751824563129));
#13550=CARTESIAN_POINT('',(-0.0042,-0.00157079633417248,0.0119999999989629));
#13551=CARTESIAN_POINT('',(-0.0042,-7.92248253258906E-12,0.012));
#13552=CARTESIAN_POINT('',(-0.00419999987509607,-2.46123798780892E-12,0.0120000000001977));
#13553=CARTESIAN_POINT('',(-0.004199999875,-4.0775188822195E-12,-0.012));
#13554=CARTESIAN_POINT('',(-0.0042,0.,-1.2166193978184E-18));
#13555=CARTESIAN_POINT('',(-0.0206375,0.,0.));
#13556=CARTESIAN_POINT('',(0.00100623059,-4.57509504672808E-12,-0.01065));
#13557=CARTESIAN_POINT('',(0.00100623059,-0.00139408174412197,-0.0106499999994011));
#13558=CARTESIAN_POINT('',(0.00100623059,-0.00418159533265356,-0.0100954744309421));
#13559=CARTESIAN_POINT('',(0.00100623059,-0.00772676506497774,-0.00772674161289855));
#13560=CARTESIAN_POINT('',(0.00100623059,-0.010095467732356,-0.00418168242818399));
#13561=CARTESIAN_POINT('',(0.00100623059,-0.0109272661335809,-1.26002854163711E-12));
#13562=CARTESIAN_POINT('',(0.00100623059,-0.0100954677333204,0.00418168242585576));
#13563=CARTESIAN_POINT('',(0.00100623059,-0.00772676506675968,0.0077267416111166));
#13564=CARTESIAN_POINT('',(0.00100623059,-0.00418159533498178,0.0100954744299777));
#13565=CARTESIAN_POINT('',(0.00100623059,-0.00139408174657808,0.0106499999990796));
#13566=CARTESIAN_POINT('',(0.00100623059,-7.03120324767279E-12,0.01065));
#13567=CARTESIAN_POINT('',(0.00100623096506661,-2.18434900175713E-12,0.0106499999996362));
#13568=CARTESIAN_POINT('',(0.00100623059006661,-4.95004771836549E-12,-0.0106499999996362));
#13569=CARTESIAN_POINT('',(0.00100623059013322,-5.59151227703387E-14,4.31770786296025E-20));
#13570=CARTESIAN_POINT('',(-0.00420000000011192,-3.50900396996374E-13,-2.29851109841953E-19));
#13571=CARTESIAN_POINT('',(-0.00450000000033692,-3.52327230154582E-13,-2.37871579129804E-19));
#13572=CARTESIAN_POINT('',(-0.00450000000039257,0.0116999999998398,-2.37871579129804E-19));
#13573=CARTESIAN_POINT('',(1.154356125671E-13,4.73423576231519E-14,5.99501471359368E-21));
#13574=CARTESIAN_POINT('',(0.00100623059013322,5.05895643960993E-20,-0.0106499999992724));
#13575=CARTESIAN_POINT('',(0.00132239692493253,3.43168701089793E-15,-0.0102965152906072));
#13576=CARTESIAN_POINT('',(0.00153614706478366,8.87052617196055E-15,-0.00923383493259741));
#13577=CARTESIAN_POINT('',(0.000724069227561596,4.32262384432489E-15,-0.00851584589933923));
#13578=CARTESIAN_POINT('',(0.000258602131639666,7.10249954130499E-18,-0.00842500002362359));
#13579=CARTESIAN_POINT('',(0.000258602136233779,-2.86275794301951E-12,-0.00842500000008472));
#13580=CARTESIAN_POINT('',(0.000258602011467558,-2.86275710191455E-12,-0.00842500000016943));
#13581=CARTESIAN_POINT('',(0.000258602011476953,-0.00110282992379344,-0.00842499999978821));
#13582=CARTESIAN_POINT('',(0.00025860201149574,-0.0033079756503873,-0.00798632601725331));
#13583=CARTESIAN_POINT('',(0.000258602011519631,-0.00611248785699539,-0.00611246930397495));
#13584=CARTESIAN_POINT('',(0.000258602011535596,-0.00798632071841419,-0.00330804454916419));
#13585=CARTESIAN_POINT('',(0.000258602011541202,-0.00864433964108412,5.82148394867342E-13));
#13586=CARTESIAN_POINT('',(0.000258602011535596,-0.00798632071796863,0.00330804455023986));
#13587=CARTESIAN_POINT('',(0.000258602011519632,-0.00611248785617209,0.00611246930479825));
#13588=CARTESIAN_POINT('',(0.000258602011495739,-0.00330797564931162,0.00798632601769886));
#13589=CARTESIAN_POINT('',(0.000258602011476953,-0.00110282992265868,0.00842499999993675));
#13590=CARTESIAN_POINT('',(0.000258602011467558,-1.72799521891854E-12,0.00842500000016943));
#13591=CARTESIAN_POINT('',(0.000258602136233782,-1.72799408318983E-12,0.00842500000008472));
#13592=CARTESIAN_POINT('',(0.000258602131639668,-2.26363092258843E-17,0.00842500002362359));
#13593=CARTESIAN_POINT('',(0.000724069186718163,4.30004688906155E-15,0.00851584589136776));
#13594=CARTESIAN_POINT('',(0.00153614696900967,8.86942973976054E-15,0.00923383480668362));
#13595=CARTESIAN_POINT('',(0.00132239699826857,3.44075559505266E-15,0.0102965150770454));
#13596=CARTESIAN_POINT('',(0.00100623075658947,1.92149073831785E-17,0.0106499998131686));
#13597=CARTESIAN_POINT('',(1.1543600703228E-13,-4.73427093034189E-14,5.83742937136908E-20));
#13598=CARTESIAN_POINT('',(0.00025860201146756,-4.95458259515107E-14,5.44685981140106E-20));
#13599=CARTESIAN_POINT('',(-0.0045,-5.3776427755281E-19,1.47451495458029E-19));
#13600=CARTESIAN_POINT('',(-0.0045,0.,0.));
#13601=CARTESIAN_POINT('',(-0.0045,0.,-0.011075));
#13602=CARTESIAN_POINT('',(-0.0206375,0.,-9.16300179894287E-52));
#13603=CARTESIAN_POINT('',(0.0045,0.,-1.98752982420284E-18));
#13604=CARTESIAN_POINT('',(0.0045,0.,-0.008425));
#13605=CARTESIAN_POINT('',(-0.0206375,0.,0.));
#13606=CARTESIAN_POINT('',(-0.000258602011,-7.31179117070199E-12,0.011075));
#13607=CARTESIAN_POINT('',(-0.000258602011,-0.00144971411674669,0.0110749999990429));
#13608=CARTESIAN_POINT('',(-0.000258602011,-0.00434846651032143,0.0104983454753055));
#13609=CARTESIAN_POINT('',(-0.000258602011,-0.00803511015158343,0.00803508575991702));
#13610=CARTESIAN_POINT('',(-0.000258602011,-0.0104983385114106,0.00434855707665283));
#13611=CARTESIAN_POINT('',(-0.000258602011,-0.0113633307445454,-1.31030853718747E-12));
#13612=CARTESIAN_POINT('',(-0.000258602011,-0.0104983385104078,-0.00434855707907396));
#13613=CARTESIAN_POINT('',(-0.000258602011,-0.00803511014973037,-0.00803508576177009));
#13614=CARTESIAN_POINT('',(-0.000258602011,-0.0043484665079003,-0.0104983454763083));
#13615=CARTESIAN_POINT('',(-0.000258602011,-0.00144971411419257,-0.0110749999993772));
#13616=CARTESIAN_POINT('',(-0.000258602011,-4.75766926220784E-12,-0.011075));
#13617=CARTESIAN_POINT('',(-0.00025860238623378,-9.94454622315446E-13,-0.0110749999999153));
#13618=CARTESIAN_POINT('',(-0.000258602071199268,-6.4246432521501E-12,0.0110749999882117));
#13619=CARTESIAN_POINT('',(-0.000258602011467561,4.51272795225522E-14,-3.71516306442422E-19));
#13620=CARTESIAN_POINT('',(0.0045,-2.22911966663019E-18,1.73472347597681E-20));
#13621=CARTESIAN_POINT('',(0.00450000000033692,3.48751202232752E-13,1.08129136841049E-19));
#13622=CARTESIAN_POINT('',(0.00450000000033692,6.37547546112859E-19,0.00779999999980785));
#13623=CARTESIAN_POINT('',(0.00450000000036139,-1.95000042881955E-12,-0.00779999999974705));
#13624=CARTESIAN_POINT('',(0.00450000000033692,-3.48751060863252E-13,-4.06296004640648E-19));
#13625=CARTESIAN_POINT('',(-1.1543990834159E-13,-4.73314002437894E-14,3.54060453998605E-19));
#13626=CARTESIAN_POINT('',(-0.0010062306454784,7.00818953022586E-18,-0.00885000006260538));
#13627=CARTESIAN_POINT('',(-0.00132239692205273,3.80617846662212E-15,-0.00920348474991875));
#13628=CARTESIAN_POINT('',(-0.00153614703263649,9.26191304452231E-15,-0.0102661649538024));
#13629=CARTESIAN_POINT('',(-0.000724069398158462,4.2080152504004E-15,-0.0109841539795411));
#13630=CARTESIAN_POINT('',(-0.000258602372466113,5.89741576151065E-17,-0.0110749999293739));
#13631=CARTESIAN_POINT('',(-0.00100623071506661,-7.94670107870803E-13,-0.0088500000003638));
#13632=CARTESIAN_POINT('',(-0.000258602011467561,1.98785142045412E-17,0.0110749999998306));
#13633=CARTESIAN_POINT('',(-0.000724069122077457,4.17825833481557E-15,0.0109841541650723));
#13634=CARTESIAN_POINT('',(-0.00153614703309098,9.25202015462542E-15,0.0102661651868448));
#13635=CARTESIAN_POINT('',(-0.00132239696292048,3.81144573458941E-15,0.0092034847956103));
#13636=CARTESIAN_POINT('',(-0.0010062306454784,1.90012882174815E-17,0.00885000006260538));
#13637=CARTESIAN_POINT('',(-0.00100623071506661,-6.59462196535367E-12,0.0088500000003638));
#13638=CARTESIAN_POINT('',(-0.00100623059013322,-6.59462086751533E-12,0.00885000000072759));
#13639=CARTESIAN_POINT('',(-0.00100623059014309,-0.00115846229739644,0.00884999999986943));
#13640=CARTESIAN_POINT('',(-0.00100623059016283,-0.00347484682895264,0.0083891970618622));
#13641=CARTESIAN_POINT('',(-0.00100623059018793,-0.0064208329443351,0.00642081345110636));
#13642=CARTESIAN_POINT('',(-0.00100623059020469,-0.00838919149809096,0.00347491919774606));
#13643=CARTESIAN_POINT('',(-0.00100623059021058,-0.00908040425267338,-2.97546799044951E-12));
#13644=CARTESIAN_POINT('',(-0.00100623059020469,-0.00838919149581363,-0.00347491920324402));
#13645=CARTESIAN_POINT('',(-0.00100623059018793,-0.00642083294012714,-0.00642081345531434));
#13646=CARTESIAN_POINT('',(-0.00100623059016283,-0.00347484682345468,-0.00838919706413948));
#13647=CARTESIAN_POINT('',(-0.00100623059014309,-0.00115846229159649,-0.00885000000062864));
#13648=CARTESIAN_POINT('',(-0.00100623059013322,-7.94669450589741E-13,-0.00885000000072759));
#13649=CARTESIAN_POINT('',(-1.1544007415132E-13,4.73304495273867E-14,-3.69660968558101E-19));
#13650=CARTESIAN_POINT('',(-0.00100623059013322,3.87578284472844E-14,-3.76880161186426E-19));
#13651=CARTESIAN_POINT('',(0.00420000000011192,-3.50891387635993E-13,-4.14898835309052E-19));
#13652=CARTESIAN_POINT('',(0.00420000000019215,8.38119770267861E-18,0.00749999999960454));
#13653=CARTESIAN_POINT('',(0.00435707963295547,-4.05846340527414E-15,0.00749999999964655));
#13654=CARTESIAN_POINT('',(0.00450000000032556,-1.62862306384024E-15,0.00764292036704453));
#13655=CARTESIAN_POINT('',(0.00450000000033692,-3.54563742746683E-19,0.00779999999980785));
#13656=CARTESIAN_POINT('',(0.00419999987517108,-1.5382740212674E-12,0.00749999999980227));
#13657=CARTESIAN_POINT('',(0.00450000000033692,-1.43886481780106E-17,-0.00779999999980785));
#13658=CARTESIAN_POINT('',(0.00450000000032556,-1.62909625669243E-15,-0.00764292036704453));
#13659=CARTESIAN_POINT('',(0.00435707963295547,-4.04642258766554E-15,-0.00749999999964655));
#13660=CARTESIAN_POINT('',(0.00420000000019215,3.31895800936513E-17,-0.00749999999960454));
#13661=CARTESIAN_POINT('',(0.00419999987509607,-4.29142485976802E-12,-0.00749999999980227));
#13662=CARTESIAN_POINT('',(0.00420000000019215,-4.29142066913366E-12,-0.00749999999960454));
#13663=CARTESIAN_POINT('',(0.00420000000020615,-0.00196349541225418,-0.00749999999857291));
#13664=CARTESIAN_POINT('',(0.00420000000023406,-0.0058748540154159,-0.00587708718402969));
#13665=CARTESIAN_POINT('',(0.00420000000025145,-0.00831257299276455,1.52571835373982E-12));
#13666=CARTESIAN_POINT('',(0.00420000000023406,-0.0058748540132585,0.00587708718618627));
#13667=CARTESIAN_POINT('',(0.00420000000020615,-0.00196349540950103,0.00749999999929369));
#13668=CARTESIAN_POINT('',(0.00420000000019215,-1.53826945716326E-12,0.00749999999960454));
#13669=CARTESIAN_POINT('',(0.00420000000011192,3.50891535870921E-13,1.16083160393565E-19));
#13670=CARTESIAN_POINT('',(0.00420000000011192,3.50891535870921E-13,1.16083160393565E-19));
#13671=CARTESIAN_POINT('',(-0.0206375,0.,0.));
#13672=CARTESIAN_POINT('',(-0.0045,0.,0.));
#13673=CARTESIAN_POINT('',(-0.0045,0.,-0.00885));
#13674=CARTESIAN_POINT('',(-0.0206375,0.,-2.47065262083525E-51));
#13675=CARTESIAN_POINT('',(-0.0042,-3.22189792023104E-12,-0.0075));
#13676=CARTESIAN_POINT('',(-0.0042,-0.0019634954110344,-0.00749999999915651));
#13677=CARTESIAN_POINT('',(-0.0042,-0.00587485401406066,-0.00587708718534322));
#13678=CARTESIAN_POINT('',(-0.0042,-0.00831257299263083,-9.5852737806285E-13));
#13679=CARTESIAN_POINT('',(-0.0042,-0.00587485401541604,0.00587708718398836));
#13680=CARTESIAN_POINT('',(-0.0042,-0.00196349541276405,0.00749999999870368));
#13681=CARTESIAN_POINT('',(-0.0042,-4.95155158286816E-12,0.0075));
#13682=CARTESIAN_POINT('',(-0.00419999962509607,-1.53827397134479E-12,0.00749999999980227));
#13683=CARTESIAN_POINT('',(-0.00420000000009607,-3.48594912388589E-12,-0.00749999999980227));
#13684=CARTESIAN_POINT('',(-0.00420000000011191,3.50891751372691E-13,2.79083595183788E-19));
#13685=CARTESIAN_POINT('',(-0.0045,-4.07660016854549E-19,-7.28583859910259E-19));
#13686=CARTESIAN_POINT('',(-0.00450000000033692,3.48751417212871E-13,2.87745340681233E-19));
#13687=CARTESIAN_POINT('',(-0.00450000000033692,-2.42388042693057E-19,-0.00779999999980785));
#13688=CARTESIAN_POINT('',(-0.00450000000036139,-1.9500002825196E-12,0.00779999999974705));
#13689=CARTESIAN_POINT('',(-0.00450000000033692,-3.48750946764454E-13,-1.41700427235676E-19));
#13690=CARTESIAN_POINT('',(-0.00420000000011191,-3.50891287789699E-13,-1.29656749332468E-19));
#13691=CARTESIAN_POINT('',(-0.00450000000033692,-2.40464944123498E-19,0.00779999999980786));
#13692=CARTESIAN_POINT('',(-0.00450000000032556,-1.62850896504167E-15,0.00764292036704453));
#13693=CARTESIAN_POINT('',(-0.00435707963295547,-4.05835609638575E-15,0.00749999999964656));
#13694=CARTESIAN_POINT('',(-0.00420000000019214,8.48104399744249E-18,0.00749999999960455));
#13695=CARTESIAN_POINT('',(-0.00420000000019214,3.32894263884152E-17,-0.00749999999960455));
#13696=CARTESIAN_POINT('',(-0.00435707963295547,-4.04631527877715E-15,-0.00749999999964656));
#13697=CARTESIAN_POINT('',(-0.00450000000032556,-1.62898215789386E-15,-0.00764292036704453));
#13698=CARTESIAN_POINT('',(-0.00450000000033692,-1.42745493793874E-17,-0.00779999999980786));
#13699=CARTESIAN_POINT('',(-0.00420000000011191,3.50891751372691E-13,2.79083595183788E-19));
#18809=MECHANICAL_DESIGN_GEOMETRIC_PRESENTATION_REPRESENTATION('',(#8178),#18810);
#18810=(
GEOMETRIC_REPRESENTATION_CONTEXT(3)
GLOBAL_UNCERTAINTY_ASSIGNED_CONTEXT((#18817))
GLOBAL_UNIT_ASSIGNED_CONTEXT((#18826,#18825,#18824))
REPRESENTATION_CONTEXT('MAS-697','TOP_LEVEL_ASSEMBLY_PART')
);
#18815=(
GEOMETRIC_REPRESENTATION_CONTEXT(3)
GLOBAL_UNCERTAINTY_ASSIGNED_CONTEXT((#18822))
GLOBAL_UNIT_ASSIGNED_CONTEXT((#18826,#18825,#18824))
REPRESENTATION_CONTEXT(
'angular contact ball bearing_68_bsi_BS 6267 ABB - 4815 - 18,SI,NC,18_
68__ DE    23193','COMPONENT_PART')
);
#18817=UNCERTAINTY_MEASURE_WITH_UNIT(LENGTH_MEASURE(1.E-8),#18826,
'DISTANCE_ACCURACY_VALUE','Maximum Tolerance applied to model');
#18822=UNCERTAINTY_MEASURE_WITH_UNIT(LENGTH_MEASURE(2.E-5),#18826,
'DISTANCE_ACCURACY_VALUE','Maximum Tolerance applied to model');
#18824=(
NAMED_UNIT(*)
SI_UNIT($,.STERADIAN.)
SOLID_ANGLE_UNIT()
);
#18825=(
NAMED_UNIT(*)
PLANE_ANGLE_UNIT()
SI_UNIT($,.RADIAN.)
);
#18826=(
LENGTH_UNIT()
NAMED_UNIT(*)
SI_UNIT($,.METRE.)
);
#18836=PRODUCT_DEFINITION_SHAPE('','',#18845);
#18845=PRODUCT_DEFINITION('','',#18859,#18852);
#18852=PRODUCT_DEFINITION_CONTEXT('',#18890,'design');
#18859=PRODUCT_DEFINITION_FORMATION_WITH_SPECIFIED_SOURCE('','',#18873,
 .NOT_KNOWN.);
#18873=PRODUCT(
'angular contact ball bearing_68_bsi_BS 6267 ABB - 4815 - 18,SI,NC,18_
68__ DE    23193',
'angular contact ball bearing_68_bsi_BS 6267 ABB - 4815 - 18,SI,NC,18_
68__ DE    23193',
'angular contact ball bearing_68_bsi_BS 6267 ABB - 4815 - 18,SI,NC,18_
68__ DE    23193',(#18887));
#18887=PRODUCT_CONTEXT('',#18890,'mechanical');
#18890=APPLICATION_CONTEXT('managed model based 3d engineering');
ENDSEC;
END-ISO-10303-21;
